ISO-10303-21;
HEADER;
/* Generated by software containing ST-Developer
 * from STEP Tools, Inc. (www.steptools.com) 
 */

FILE_DESCRIPTION(
/* description */ (''),
/* implementation_level */ '2;1');

FILE_NAME(
/* name */ 'Nut_01.step',
/* time_stamp */ '2026-11-14T03:52:36-08:00',
/* author */ (''),
/* organization */ (''),
/* preprocessor_version */ 'ST-DEVELOPER v20.2',
/* originating_system */ 'Autodesk Translation Framework v15.17.0.0',
/* authorisation */ '');

FILE_SCHEMA (('AUTOMOTIVE_DESIGN { 1 0 10303 214 3 1 1 }'));
ENDSEC;

DATA;
#10=MECHANICAL_DESIGN_GEOMETRIC_PRESENTATION_REPRESENTATION('',(#196),#19443);
#180=SHAPE_REPRESENTATION_RELATIONSHIP('SRR','None',#19480,#188);
#188=ADVANCED_BREP_SHAPE_REPRESENTATION('',(#204),#19440);
#196=STYLED_ITEM('',(#19525),#204);
#204=MANIFOLD_SOLID_BREP('Body1',#2023);
#216=FACE_BOUND('',#457,.T.);
#217=FACE_BOUND('',#459,.T.);
#251=PLANE('',#2224);
#252=PLANE('',#2225);
#253=PLANE('',#2226);
#254=PLANE('',#2227);
#255=PLANE('',#2228);
#256=PLANE('',#2229);
#257=PLANE('',#2230);
#258=PLANE('',#2231);
#344=FACE_OUTER_BOUND('',#449,.T.);
#345=FACE_OUTER_BOUND('',#450,.T.);
#346=FACE_OUTER_BOUND('',#451,.T.);
#347=FACE_OUTER_BOUND('',#452,.T.);
#348=FACE_OUTER_BOUND('',#453,.T.);
#349=FACE_OUTER_BOUND('',#454,.T.);
#350=FACE_OUTER_BOUND('',#455,.T.);
#351=FACE_OUTER_BOUND('',#456,.T.);
#352=FACE_OUTER_BOUND('',#458,.T.);
#449=EDGE_LOOP('',(#1771,#1772,#1773,#1774));
#450=EDGE_LOOP('',(#1775,#1776,#1777,#1778));
#451=EDGE_LOOP('',(#1779,#1780,#1781,#1782));
#452=EDGE_LOOP('',(#1783,#1784,#1785,#1786));
#453=EDGE_LOOP('',(#1787,#1788,#1789,#1790));
#454=EDGE_LOOP('',(#1791,#1792,#1793,#1794));
#455=EDGE_LOOP('',(#1795,#1796,#1797,#1798));
#456=EDGE_LOOP('',(#1799,#1800,#1801,#1802,#1803,#1804));
#457=EDGE_LOOP('',(#1805));
#458=EDGE_LOOP('',(#1806,#1807,#1808,#1809,#1810,#1811));
#459=EDGE_LOOP('',(#1812));
#558=LINE('',#19298,#685);
#559=LINE('',#19303,#686);
#560=LINE('',#19305,#687);
#561=LINE('',#19307,#688);
#562=LINE('',#19308,#689);
#563=LINE('',#19311,#690);
#564=LINE('',#19313,#691);
#565=LINE('',#19314,#692);
#566=LINE('',#19317,#693);
#567=LINE('',#19319,#694);
#568=LINE('',#19320,#695);
#569=LINE('',#19323,#696);
#570=LINE('',#19325,#697);
#571=LINE('',#19326,#698);
#572=LINE('',#19329,#699);
#573=LINE('',#19331,#700);
#574=LINE('',#19332,#701);
#575=LINE('',#19334,#702);
#576=LINE('',#19335,#703);
#685=VECTOR('',#2562,2.942);
#686=VECTOR('',#2567,10.);
#687=VECTOR('',#2568,10.);
#688=VECTOR('',#2569,10.);
#689=VECTOR('',#2570,10.);
#690=VECTOR('',#2573,10.);
#691=VECTOR('',#2574,10.);
#692=VECTOR('',#2575,10.);
#693=VECTOR('',#2578,10.);
#694=VECTOR('',#2579,10.);
#695=VECTOR('',#2580,10.);
#696=VECTOR('',#2583,10.);
#697=VECTOR('',#2584,10.);
#698=VECTOR('',#2585,10.);
#699=VECTOR('',#2588,10.);
#700=VECTOR('',#2589,10.);
#701=VECTOR('',#2590,10.);
#702=VECTOR('',#2593,10.);
#703=VECTOR('',#2594,10.);
#766=CIRCLE('',#2222,2.942);
#767=CIRCLE('',#2223,2.942);
#956=VERTEX_POINT('',#19295);
#957=VERTEX_POINT('',#19297);
#958=VERTEX_POINT('',#19301);
#959=VERTEX_POINT('',#19302);
#960=VERTEX_POINT('',#19304);
#961=VERTEX_POINT('',#19306);
#962=VERTEX_POINT('',#19310);
#963=VERTEX_POINT('',#19312);
#964=VERTEX_POINT('',#19316);
#965=VERTEX_POINT('',#19318);
#966=VERTEX_POINT('',#19322);
#967=VERTEX_POINT('',#19324);
#968=VERTEX_POINT('',#19328);
#969=VERTEX_POINT('',#19330);
#1234=EDGE_CURVE('',#956,#956,#766,.T.);
#1235=EDGE_CURVE('',#956,#957,#558,.T.);
#1236=EDGE_CURVE('',#957,#957,#767,.T.);
#1237=EDGE_CURVE('',#958,#959,#559,.T.);
#1238=EDGE_CURVE('',#959,#960,#560,.T.);
#1239=EDGE_CURVE('',#961,#960,#561,.T.);
#1240=EDGE_CURVE('',#958,#961,#562,.T.);
#1241=EDGE_CURVE('',#962,#958,#563,.T.);
#1242=EDGE_CURVE('',#963,#961,#564,.T.);
#1243=EDGE_CURVE('',#962,#963,#565,.T.);
#1244=EDGE_CURVE('',#964,#962,#566,.T.);
#1245=EDGE_CURVE('',#965,#963,#567,.T.);
#1246=EDGE_CURVE('',#964,#965,#568,.T.);
#1247=EDGE_CURVE('',#966,#964,#569,.T.);
#1248=EDGE_CURVE('',#967,#965,#570,.T.);
#1249=EDGE_CURVE('',#966,#967,#571,.T.);
#1250=EDGE_CURVE('',#968,#966,#572,.T.);
#1251=EDGE_CURVE('',#969,#967,#573,.T.);
#1252=EDGE_CURVE('',#968,#969,#574,.T.);
#1253=EDGE_CURVE('',#959,#968,#575,.T.);
#1254=EDGE_CURVE('',#960,#969,#576,.T.);
#1771=ORIENTED_EDGE('',*,*,#1234,.T.);
#1772=ORIENTED_EDGE('',*,*,#1235,.T.);
#1773=ORIENTED_EDGE('',*,*,#1236,.F.);
#1774=ORIENTED_EDGE('',*,*,#1235,.F.);
#1775=ORIENTED_EDGE('',*,*,#1237,.T.);
#1776=ORIENTED_EDGE('',*,*,#1238,.T.);
#1777=ORIENTED_EDGE('',*,*,#1239,.F.);
#1778=ORIENTED_EDGE('',*,*,#1240,.F.);
#1779=ORIENTED_EDGE('',*,*,#1241,.T.);
#1780=ORIENTED_EDGE('',*,*,#1240,.T.);
#1781=ORIENTED_EDGE('',*,*,#1242,.F.);
#1782=ORIENTED_EDGE('',*,*,#1243,.F.);
#1783=ORIENTED_EDGE('',*,*,#1244,.T.);
#1784=ORIENTED_EDGE('',*,*,#1243,.T.);
#1785=ORIENTED_EDGE('',*,*,#1245,.F.);
#1786=ORIENTED_EDGE('',*,*,#1246,.F.);
#1787=ORIENTED_EDGE('',*,*,#1247,.T.);
#1788=ORIENTED_EDGE('',*,*,#1246,.T.);
#1789=ORIENTED_EDGE('',*,*,#1248,.F.);
#1790=ORIENTED_EDGE('',*,*,#1249,.F.);
#1791=ORIENTED_EDGE('',*,*,#1250,.T.);
#1792=ORIENTED_EDGE('',*,*,#1249,.T.);
#1793=ORIENTED_EDGE('',*,*,#1251,.F.);
#1794=ORIENTED_EDGE('',*,*,#1252,.F.);
#1795=ORIENTED_EDGE('',*,*,#1253,.T.);
#1796=ORIENTED_EDGE('',*,*,#1252,.T.);
#1797=ORIENTED_EDGE('',*,*,#1254,.F.);
#1798=ORIENTED_EDGE('',*,*,#1238,.F.);
#1799=ORIENTED_EDGE('',*,*,#1254,.T.);
#1800=ORIENTED_EDGE('',*,*,#1251,.T.);
#1801=ORIENTED_EDGE('',*,*,#1248,.T.);
#1802=ORIENTED_EDGE('',*,*,#1245,.T.);
#1803=ORIENTED_EDGE('',*,*,#1242,.T.);
#1804=ORIENTED_EDGE('',*,*,#1239,.T.);
#1805=ORIENTED_EDGE('',*,*,#1236,.T.);
#1806=ORIENTED_EDGE('',*,*,#1253,.F.);
#1807=ORIENTED_EDGE('',*,*,#1237,.F.);
#1808=ORIENTED_EDGE('',*,*,#1241,.F.);
#1809=ORIENTED_EDGE('',*,*,#1244,.F.);
#1810=ORIENTED_EDGE('',*,*,#1247,.F.);
#1811=ORIENTED_EDGE('',*,*,#1250,.F.);
#1812=ORIENTED_EDGE('',*,*,#1234,.F.);
#1919=CYLINDRICAL_SURFACE('',#2221,2.942);
#1993=ADVANCED_FACE('',(#344),#1919,.F.);
#1994=ADVANCED_FACE('',(#345),#251,.T.);
#1995=ADVANCED_FACE('',(#346),#252,.T.);
#1996=ADVANCED_FACE('',(#347),#253,.T.);
#1997=ADVANCED_FACE('',(#348),#254,.T.);
#1998=ADVANCED_FACE('',(#349),#255,.T.);
#1999=ADVANCED_FACE('',(#350),#256,.T.);
#2000=ADVANCED_FACE('',(#351,#216),#257,.T.);
#2001=ADVANCED_FACE('',(#352,#217),#258,.F.);
#2023=CLOSED_SHELL('',(#1993,#1994,#1995,#1996,#1997,#1998,#1999,#2000,
#2001));
#2220=AXIS2_PLACEMENT_3D('',#19293,#2556,#2557);
#2221=AXIS2_PLACEMENT_3D('',#19294,#2558,#2559);
#2222=AXIS2_PLACEMENT_3D('',#19296,#2560,#2561);
#2223=AXIS2_PLACEMENT_3D('',#19299,#2563,#2564);
#2224=AXIS2_PLACEMENT_3D('',#19300,#2565,#2566);
#2225=AXIS2_PLACEMENT_3D('',#19309,#2571,#2572);
#2226=AXIS2_PLACEMENT_3D('',#19315,#2576,#2577);
#2227=AXIS2_PLACEMENT_3D('',#19321,#2581,#2582);
#2228=AXIS2_PLACEMENT_3D('',#19327,#2586,#2587);
#2229=AXIS2_PLACEMENT_3D('',#19333,#2591,#2592);
#2230=AXIS2_PLACEMENT_3D('',#19336,#2595,#2596);
#2231=AXIS2_PLACEMENT_3D('',#19337,#2597,#2598);
#2556=DIRECTION('axis',(0.,0.,1.));
#2557=DIRECTION('refdir',(1.,0.,0.));
#2558=DIRECTION('center_axis',(0.,0.,1.));
#2559=DIRECTION('ref_axis',(-1.,0.,0.));
#2560=DIRECTION('center_axis',(0.,0.,-1.));
#2561=DIRECTION('ref_axis',(-1.,0.,0.));
#2562=DIRECTION('',(0.,0.,1.));
#2563=DIRECTION('center_axis',(0.,0.,-1.));
#2564=DIRECTION('ref_axis',(-1.,0.,0.));
#2565=DIRECTION('center_axis',(-0.866025403784439,-0.5,0.));
#2566=DIRECTION('ref_axis',(0.5,-0.866025403784439,0.));
#2567=DIRECTION('',(0.5,-0.866025403784439,0.));
#2568=DIRECTION('',(0.,0.,1.));
#2569=DIRECTION('',(0.5,-0.866025403784439,0.));
#2570=DIRECTION('',(0.,0.,1.));
#2571=DIRECTION('center_axis',(-0.866025403784439,0.5,0.));
#2572=DIRECTION('ref_axis',(-0.5,-0.866025403784439,0.));
#2573=DIRECTION('',(-0.5,-0.866025403784439,0.));
#2574=DIRECTION('',(-0.5,-0.866025403784439,0.));
#2575=DIRECTION('',(0.,0.,1.));
#2576=DIRECTION('center_axis',(1.20185167898973E-16,1.,0.));
#2577=DIRECTION('ref_axis',(-1.,1.20185167898973E-16,0.));
#2578=DIRECTION('',(-1.,1.20185167898973E-16,0.));
#2579=DIRECTION('',(-1.,1.20185167898973E-16,0.));
#2580=DIRECTION('',(0.,0.,1.));
#2581=DIRECTION('center_axis',(0.866025403784439,0.5,0.));
#2582=DIRECTION('ref_axis',(-0.5,0.866025403784439,0.));
#2583=DIRECTION('',(-0.5,0.866025403784439,0.));
#2584=DIRECTION('',(-0.5,0.866025403784439,0.));
#2585=DIRECTION('',(0.,0.,1.));
#2586=DIRECTION('center_axis',(0.866025403784439,-0.5,0.));
#2587=DIRECTION('ref_axis',(0.5,0.866025403784439,0.));
#2588=DIRECTION('',(0.5,0.866025403784439,0.));
#2589=DIRECTION('',(0.5,0.866025403784439,0.));
#2590=DIRECTION('',(0.,0.,1.));
#2591=DIRECTION('center_axis',(2.40370335797945E-16,-1.,0.));
#2592=DIRECTION('ref_axis',(1.,2.40370335797945E-16,0.));
#2593=DIRECTION('',(1.,2.40370335797945E-16,0.));
#2594=DIRECTION('',(1.,2.40370335797945E-16,0.));
#2595=DIRECTION('center_axis',(0.,0.,1.));
#2596=DIRECTION('ref_axis',(-1.,0.,0.));
#2597=DIRECTION('center_axis',(0.,0.,1.));
#2598=DIRECTION('ref_axis',(-1.,0.,0.));
#19293=CARTESIAN_POINT('',(0.,0.,0.));
#19294=CARTESIAN_POINT('Origin',(-33.7561270252576,0.,309.));
#19295=CARTESIAN_POINT('',(-30.8141270252576,3.60291088309151E-16,309.));
#19296=CARTESIAN_POINT('Origin',(-33.7561270252576,0.,309.));
#19297=CARTESIAN_POINT('',(-30.8141270252576,3.60291088309151E-16,312.));
#19298=CARTESIAN_POINT('',(-30.8141270252576,3.60291088309151E-16,309.));
#19299=CARTESIAN_POINT('Origin',(-33.7561270252576,0.,312.));
#19300=CARTESIAN_POINT('Origin',(-38.3749291787746,8.32667268468867E-16,
309.));
#19301=CARTESIAN_POINT('',(-38.3749291787746,8.32667268468867E-16,309.));
#19302=CARTESIAN_POINT('',(-36.0655281020161,-4.,309.));
#19303=CARTESIAN_POINT('',(-38.3749291787746,8.32667268468867E-16,309.));
#19304=CARTESIAN_POINT('',(-36.0655281020161,-4.,312.));
#19305=CARTESIAN_POINT('',(-36.0655281020161,-4.,309.));
#19306=CARTESIAN_POINT('',(-38.3749291787746,8.32667268468867E-16,312.));
#19307=CARTESIAN_POINT('',(-38.3749291787746,8.32667268468867E-16,312.));
#19308=CARTESIAN_POINT('',(-38.3749291787746,8.32667268468867E-16,309.));
#19309=CARTESIAN_POINT('Origin',(-36.0655281020161,4.,309.));
#19310=CARTESIAN_POINT('',(-36.0655281020161,4.,309.));
#19311=CARTESIAN_POINT('',(-36.0655281020161,4.,309.));
#19312=CARTESIAN_POINT('',(-36.0655281020161,4.,312.));
#19313=CARTESIAN_POINT('',(-36.0655281020161,4.,312.));
#19314=CARTESIAN_POINT('',(-36.0655281020161,4.,309.));
#19315=CARTESIAN_POINT('Origin',(-31.4467259484991,4.,309.));
#19316=CARTESIAN_POINT('',(-31.4467259484991,4.,309.));
#19317=CARTESIAN_POINT('',(-31.4467259484991,4.,309.));
#19318=CARTESIAN_POINT('',(-31.4467259484991,4.,312.));
#19319=CARTESIAN_POINT('',(-31.4467259484991,4.,312.));
#19320=CARTESIAN_POINT('',(-31.4467259484991,4.,309.));
#19321=CARTESIAN_POINT('Origin',(-29.1373248717406,2.77555756156289E-16,
309.));
#19322=CARTESIAN_POINT('',(-29.1373248717406,2.77555756156289E-16,309.));
#19323=CARTESIAN_POINT('',(-29.1373248717406,2.77555756156289E-16,309.));
#19324=CARTESIAN_POINT('',(-29.1373248717406,2.77555756156289E-16,312.));
#19325=CARTESIAN_POINT('',(-29.1373248717406,2.77555756156289E-16,312.));
#19326=CARTESIAN_POINT('',(-29.1373248717406,2.77555756156289E-16,309.));
#19327=CARTESIAN_POINT('Origin',(-31.4467259484991,-4.,309.));
#19328=CARTESIAN_POINT('',(-31.4467259484991,-4.,309.));
#19329=CARTESIAN_POINT('',(-31.4467259484991,-4.,309.));
#19330=CARTESIAN_POINT('',(-31.4467259484991,-4.,312.));
#19331=CARTESIAN_POINT('',(-31.4467259484991,-4.,312.));
#19332=CARTESIAN_POINT('',(-31.4467259484991,-4.,309.));
#19333=CARTESIAN_POINT('Origin',(-36.0655281020161,-4.,309.));
#19334=CARTESIAN_POINT('',(-36.0655281020161,-4.,309.));
#19335=CARTESIAN_POINT('',(-36.0655281020161,-4.,312.));
#19336=CARTESIAN_POINT('Origin',(-33.7561270252576,5.55111512312578E-16,
312.));
#19337=CARTESIAN_POINT('Origin',(-33.7561270252576,5.55111512312578E-16,
309.));
#19430=UNCERTAINTY_MEASURE_WITH_UNIT(LENGTH_MEASURE(0.01),#19444,
'DISTANCE_ACCURACY_VALUE',
'Maximum model space distance between geometric entities at asserted c
onnectivities');
#19433=UNCERTAINTY_MEASURE_WITH_UNIT(LENGTH_MEASURE(0.01),#19444,
'DISTANCE_ACCURACY_VALUE',
'Maximum model space distance between geometric entities at asserted c
onnectivities');
#19440=(
GEOMETRIC_REPRESENTATION_CONTEXT(3)
GLOBAL_UNCERTAINTY_ASSIGNED_CONTEXT((#19430))
GLOBAL_UNIT_ASSIGNED_CONTEXT((#19444,#19446,#19447))
REPRESENTATION_CONTEXT('','3D')
);
#19443=(
GEOMETRIC_REPRESENTATION_CONTEXT(3)
GLOBAL_UNCERTAINTY_ASSIGNED_CONTEXT((#19433))
GLOBAL_UNIT_ASSIGNED_CONTEXT((#19444,#19446,#19447))
REPRESENTATION_CONTEXT('','3D')
);
#19444=(
LENGTH_UNIT()
NAMED_UNIT(*)
SI_UNIT(.MILLI.,.METRE.)
);
#19446=(
NAMED_UNIT(*)
PLANE_ANGLE_UNIT()
SI_UNIT($,.RADIAN.)
);
#19447=(
NAMED_UNIT(*)
SI_UNIT($,.STERADIAN.)
SOLID_ANGLE_UNIT()
);
#19454=SHAPE_DEFINITION_REPRESENTATION(#19463,#19480);
#19463=PRODUCT_DEFINITION_SHAPE('',$,#19490);
#19480=SHAPE_REPRESENTATION('',(#2220),#19440);
#19483=PRODUCT_DEFINITION_CONTEXT('part definition',#19512,'design');
#19490=PRODUCT_DEFINITION('Nut_01','Nut_01',#19499,#19483);
#19499=PRODUCT_DEFINITION_FORMATION('',$,#19520);
#19512=APPLICATION_CONTEXT(
'Core Data for Automotive Mechanical Design Process');
#19513=PRODUCT_CONTEXT('part definition',#19512,'mechanical');
#19520=PRODUCT('Nut_01','Nut_01',$,(#19513));
#19525=PRESENTATION_STYLE_ASSIGNMENT((#19528));
#19528=SURFACE_STYLE_USAGE(.BOTH.,#19531);
#19531=SURFACE_SIDE_STYLE('',(#19534));
#19534=SURFACE_STYLE_FILL_AREA(#19537);
#19537=FILL_AREA_STYLE('Opaque(160,160,160)',(#19540));
#19540=FILL_AREA_STYLE_COLOUR('Opaque(160,160,160)',#19543);
#19543=COLOUR_RGB('Opaque(160,160,160)',0.627450980392157,0.627450980392157,
0.627450980392157);
ENDSEC;
END-ISO-10303-21;
